ISO-10303-21;
HEADER;
FILE_DESCRIPTION (('STEP AP214'),
    '1' );
FILE_NAME ('hex bolt gradeab fine_iso_ISO 8765 - M8x1.0 x 40 x 22-N.step',
    '2026-10-21T18:33:49',
    ( '' ),
    ( '' ),
    'SwSTEP 2.0',
    'SolidWorks 2025',
    '' );
FILE_SCHEMA (( 'AUTOMOTIVE_DESIGN' ));
ENDSEC;

DATA;
#1=ORIENTED_EDGE ( 'NONE', *, *, #1823, .F. ) ;
#2=EDGE_CURVE ( 'NONE', #15837, #10059, #9983, .T. ) ;
#6=CARTESIAN_POINT ( 'NONE',  ( 0.01372220897669153110, -5.309964801958256153, 3.802871176606155590 ) ) ;
#23=VECTOR ( 'NONE', #5591, 1000.000000000000000 ) ;
#84=MANIFOLD_SOLID_BREP ( 'HeadFillet', #15945 ) ;
#110=AXIS2_PLACEMENT_3D ( 'NONE', #2783, #3985, #15597 ) ;
#124=AXIS2_PLACEMENT_3D ( 'NONE', #9916, #7194, #14307 ) ;
#128=EDGE_CURVE ( 'NONE', #7354, #7590, #10341, .T. ) ;
#171=EDGE_LOOP ( 'NONE', ( #9125, #326, #2269 ) ) ;
#181=SHAPE_REPRESENTATION_RELATIONSHIP ( 'NONE' , 'NONE' ,  #5501, #12175 ) ;
#190=ORIENTED_EDGE ( 'NONE', *, *, #16753, .F. ) ;
#227=DIRECTION ( 'NONE',  ( 1.000000000000000000, 0.000000000000000000, 0.000000000000000000 ) ) ;
#269=DIRECTION ( 'NONE',  ( 0.000000000000000000, -2.775557561562874095E-16, 1.000000000000000000 ) ) ;
#283=AXIS2_PLACEMENT_3D ( 'NONE', #4428, #227, #10141 ) ;
#310=ORIENTED_EDGE ( 'NONE', *, *, #17032, .T. ) ;
#326=ORIENTED_EDGE ( 'NONE', *, *, #2755, .T. ) ;
#388=ORIENTED_EDGE ( 'NONE', *, *, #15999, .F. ) ;
#391=ORIENTED_EDGE ( 'NONE', *, *, #17491, .F. ) ;
#424=CARTESIAN_POINT ( 'NONE',  ( 0.000000000000000000, -4.857225732735059864E-14, 6.500000000000037303 ) ) ;
#451=DIRECTION ( 'NONE',  ( 0.000000000000000000, -5.551115123125748189E-17, -1.000000000000000000 ) ) ;
#453=CARTESIAN_POINT ( 'NONE',  ( 4.699999999999995737, 5.629165124598635828, -3.250000000000016875 ) ) ;
#479=CARTESIAN_POINT ( 'NONE',  ( 0.5805565836007609004, 3.752776749732559924, -6.500000000000061284 ) ) ;
#497=DIRECTION ( 'NONE',  ( -1.000000000000000000, 0.000000000000000000, 0.000000000000000000 ) ) ;
#541=DIRECTION ( 'NONE',  ( -1.000000000000000000, 0.000000000000000000, 0.000000000000000000 ) ) ;
#602=ORIENTED_EDGE ( 'NONE', *, *, #17269, .T. ) ;
#612=VECTOR ( 'NONE', #541, 1000.000000000000000 ) ;
#646=VERTEX_POINT ( 'NONE', #12557 ) ;
#720=AXIS2_PLACEMENT_3D ( 'NONE', #17412, #15835, #3025 ) ;
#747=AXIS2_PLACEMENT_3D ( 'NONE', #4168, #2377, #13908 ) ;
#756=ORIENTED_EDGE ( 'NONE', *, *, #11242, .F. ) ;
#764=CIRCLE ( 'NONE', #13025, 4.400000000000027889 ) ;
#796=PLANE ( 'NONE',  #1250 ) ;
#820=EDGE_CURVE ( 'NONE', #14582, #7975, #4478, .T. ) ;
#850=VERTEX_POINT ( 'NONE', #6064 ) ;
#871=EDGE_CURVE ( 'NONE', #11023, #3553, #4318, .T. ) ;
#884=CARTESIAN_POINT ( 'NONE',  ( 4.699999999999995737, 0.000000000000000000, 0.000000000000000000 ) ) ;
#893=CARTESIAN_POINT ( 'NONE',  ( 4.699999999999995737, 3.752776749732559924, -6.500000000000061284 ) ) ;
#941=B_SPLINE_CURVE_WITH_KNOTS ( 'NONE', 3,
 ( #7293, #1757, #10102, #8611, #7381, #17372 ),
 .UNSPECIFIED., .F., .F.,
 ( 4, 2, 4 ),
 ( 0.01067228061038553305, 0.01257272967564230723, 0.01447317874089908314 ),
 .UNSPECIFIED. ) ;
#948=EDGE_LOOP ( 'NONE', ( #10716, #16047, #16495, #5680 ) ) ;
#997=AXIS2_PLACEMENT_3D ( 'NONE', #1387, #2599, #12718 ) ;
#1036=CARTESIAN_POINT ( 'NONE',  ( 0.1061556211655283882, 6.421950209808267473, 1.876855952934465721 ) ) ;
#1037=DIRECTION ( 'NONE',  ( 0.000000000000000000, -5.551115123125748189E-17, -1.000000000000000000 ) ) ;
#1050=EDGE_LOOP ( 'NONE', ( #14252, #1714, #1805 ) ) ;
#1103=CARTESIAN_POINT ( 'NONE',  ( 0.000000000000000000, 0.000000000000000000, 0.000000000000000000 ) ) ;
#1126=CARTESIAN_POINT ( 'NONE',  ( 2.027458062547893923E-14, 0.6351314446023053062, -6.500000000000062172 ) ) ;
#1134=DIRECTION ( 'NONE',  ( 1.000000000000000000, 0.000000000000000000, 0.000000000000000000 ) ) ;
#1143=CARTESIAN_POINT ( 'NONE',  ( 45.30000000000000426, 0.000000000000000000, 0.000000000000000000 ) ) ;
#1159=ADVANCED_FACE ( 'NONE', ( #3917 ), #13599, .T. ) ;
#1169=ORIENTED_EDGE ( 'NONE', *, *, #11243, .T. ) ;
#1195=LINE ( 'NONE', #16991, #9386 ) ;
#1211=CARTESIAN_POINT ( 'NONE',  ( 0.01372220897670155954, -5.948365447239731374, -2.697128823393899477 ) ) ;
#1217=CARTESIAN_POINT ( 'NONE',  ( 0.2595206531158619767, 2.531175536751702371, -6.500000000000062172 ) ) ;
#1248=EDGE_LOOP ( 'NONE', ( #2491, #7327, #310, #9857 ) ) ;
#1250=AXIS2_PLACEMENT_3D ( 'NONE', #6483, #12205, #17896 ) ;
#1279=AXIS2_PLACEMENT_3D ( 'NONE', #14376, #3231, #11579 ) ;
#1285=EDGE_CURVE ( 'NONE', #12345, #7975, #2857, .T. ) ;
#1323=DIRECTION ( 'NONE',  ( -1.000000000000000000, 0.000000000000000000, 0.000000000000000000 ) ) ;
#1331=ORIENTED_EDGE ( 'NONE', *, *, #3219, .F. ) ;
#1332=DIRECTION ( 'NONE',  ( 0.000000000000000000, -5.551115123125748189E-17, -1.000000000000000000 ) ) ;
#1340=CARTESIAN_POINT ( 'NONE',  ( 0.000000000000000000, -5.629165124598954684, 3.250000000000013323 ) ) ;
#1357=VERTEX_POINT ( 'NONE', #12218 ) ;
#1365=AXIS2_PLACEMENT_3D ( 'NONE', #4201, #2708, #5314 ) ;
#1387=CARTESIAN_POINT ( 'NONE',  ( 44.74549999999999272, 0.000000000000000000, 0.000000000000000000 ) ) ;
#1402=EDGE_CURVE ( 'NONE', #17364, #4210, #4343, .T. ) ;
#1415=EDGE_CURVE ( 'NONE', #7975, #10340, #3847, .T. ) ;
#1429=ORIENTED_EDGE ( 'NONE', *, *, #11980, .F. ) ;
#1442=FACE_OUTER_BOUND ( 'NONE', #9097, .T. ) ;
#1493=CARTESIAN_POINT ( 'NONE',  ( 45.30000000000000426, 1.912636715672988680E-16, 3.445500000000021767 ) ) ;
#1506=EDGE_CURVE ( 'NONE', #11023, #8947, #5547, .T. ) ;
#1580=DIRECTION ( 'NONE',  ( 0.000000000000000000, 5.551115123125747573E-17, 1.000000000000000000 ) ) ;
#1584=AXIS2_PLACEMENT_3D ( 'NONE', #10488, #5054, #17786 ) ;
#1614=FACE_OUTER_BOUND ( 'NONE', #6932, .T. ) ;
#1630=VECTOR ( 'NONE', #11480, 1000.000000000000000 ) ;
#1635=VECTOR ( 'NONE', #9124, 1000.000000000000000 ) ;
#1661=VERTEX_POINT ( 'NONE', #14573 ) ;
#1675=LINE ( 'NONE', #15728, #4539 ) ;
#1690=DIRECTION ( 'NONE',  ( -1.000000000000000000, 0.000000000000000000, 0.000000000000000000 ) ) ;
#1714=ORIENTED_EDGE ( 'NONE', *, *, #10903, .T. ) ;
#1723=( NAMED_UNIT ( * ) PLANE_ANGLE_UNIT ( ) SI_UNIT ( $, .RADIAN. ) );
#1741=ORIENTED_EDGE ( 'NONE', *, *, #11659, .T. ) ;
#1757=CARTESIAN_POINT ( 'NONE',  ( -1.219346279219927580E-14, 0.6351314446024779459, 6.499999999999983125 ) ) ;
#1761=B_SPLINE_CURVE_WITH_KNOTS ( 'NONE', 3,
 ( #11746, #7528, #4531, #3226, #11921, #424 ),
 .UNSPECIFIED., .F., .F.,
 ( 4, 2, 4 ),
 ( 0.006874058789394440171, 0.008773169699889987044, 0.01067228061038553305 ),
 .UNSPECIFIED. ) ;
#1764=CARTESIAN_POINT ( 'NONE',  ( 5.299999999999998934, 3.752776749732559924, -6.500000000000061284 ) ) ;
#1805=ORIENTED_EDGE ( 'NONE', *, *, #15999, .T. ) ;
#1823=EDGE_CURVE ( 'NONE', #7590, #10723, #13722, .T. ) ;
#1857=DIRECTION ( 'NONE',  ( 0.000000000000000000, -1.000000000000000000, -2.775557561562874095E-16 ) ) ;
#1860=AXIS2_PLACEMENT_3D ( 'NONE', #14608, #16017, #12864 ) ;
#1874=CARTESIAN_POINT ( 'NONE',  ( 5.699999999999996625, 0.000000000000000000, 0.000000000000000000 ) ) ;
#1940=EDGE_LOOP ( 'NONE', ( #1, #17282, #9831, #15588, #12337, #9495 ) ) ;
#2022=APPLICATION_CONTEXT ( 'automotive_design' ) ;
#2108=DIRECTION ( 'NONE',  ( 0.000000000000000000, -1.000000000000000000, 3.330669073875448914E-16 ) ) ;
#2138=VECTOR ( 'NONE', #3851, 1000.000000000000000 ) ;
#2222=CIRCLE ( 'NONE', #7308, 6.500000000000039968 ) ;
#2250=EDGE_CURVE ( 'NONE', #18326, #9192, #5608, .T. ) ;
#2269=ORIENTED_EDGE ( 'NONE', *, *, #17911, .T. ) ;
#2275=ORIENTED_EDGE ( 'NONE', *, *, #16092, .F. ) ;
#2285=CARTESIAN_POINT ( 'NONE',  ( 0.5805565836007609004, -3.752776749732685158, 6.500000000000043521 ) ) ;
#2352=DIRECTION ( 'NONE',  ( -1.000000000000000000, 0.000000000000000000, 0.000000000000000000 ) ) ;
#2353=EDGE_LOOP ( 'NONE', ( #11971, #7688, #1169, #7959 ) ) ;
#2365=DIRECTION ( 'NONE',  ( 1.000000000000000000, 0.000000000000000000, 0.000000000000000000 ) ) ;
#2369=DIRECTION ( 'NONE',  ( 0.000000000000000000, 5.551115123125747573E-17, 1.000000000000000000 ) ) ;
#2377=DIRECTION ( 'NONE',  ( 1.000000000000000000, 0.000000000000000000, 0.000000000000000000 ) ) ;
#2425=AXIS2_PLACEMENT_3D ( 'NONE', #16211, #16392, #9481 ) ;
#2438=ORIENTED_EDGE ( 'NONE', *, *, #6742, .T. ) ;
#2473=ORIENTED_EDGE ( 'NONE', *, *, #11659, .F. ) ;
#2491=ORIENTED_EDGE ( 'NONE', *, *, #6258, .F. ) ;
#2528=CARTESIAN_POINT ( 'NONE',  ( 0.01372220897661185005, 5.948365447239559067, 2.697128823393907471 ) ) ;
#2550=UNCERTAINTY_MEASURE_WITH_UNIT (LENGTH_MEASURE( 1.000000000000000082E-05 ), #13330, 'distance_accuracy_value', 'NONE');
#2571=EDGE_CURVE ( 'NONE', #12287, #1357, #8781, .T. ) ;
#2599=DIRECTION ( 'NONE',  ( -1.000000000000000000, 0.000000000000000000, 0.000000000000000000 ) ) ;
#2628=EDGE_CURVE ( 'NONE', #4375, #9885, #17739, .T. ) ;
#2644=FACE_OUTER_BOUND ( 'NONE', #12760, .T. ) ;
#2680=CARTESIAN_POINT ( 'NONE',  ( 45.30000000000000426, 2.306883830789244121E-16, -3.445500000000021767 ) ) ;
#2708=DIRECTION ( 'NONE',  ( 1.000000000000000000, 0.000000000000000000, 0.000000000000000000 ) ) ;
#2734=CARTESIAN_POINT ( 'NONE',  ( 0.5805565836007747782, -7.505553499465293932, 1.040834085586084257E-14 ) ) ;
#2755=EDGE_CURVE ( 'NONE', #646, #8947, #7522, .T. ) ;
#2757=ORIENTED_EDGE ( 'NONE', *, *, #11242, .T. ) ;
#2783=CARTESIAN_POINT ( 'NONE',  ( 4.699999999999995737, 0.000000000000000000, 0.000000000000000000 ) ) ;
#2808=CARTESIAN_POINT ( 'NONE',  ( 0.1061556211656219523, -6.421950209808431786, -1.876855952934466387 ) ) ;
#2828=MECHANICAL_DESIGN_GEOMETRIC_PRESENTATION_REPRESENTATION('',(#10581),#5497);
#2857=CIRCLE ( 'NONE', #13026, 6.500000000000039968 ) ;
#2876=DIRECTION ( 'NONE',  ( -1.000000000000000000, -0.000000000000000000, -0.000000000000000000 ) ) ;
#2877=EDGE_LOOP ( 'NONE', ( #11890, #16937, #6354 ) ) ;
#2950=CARTESIAN_POINT ( 'NONE',  ( 4.699999999999995737, 7.505553499465141165, -1.387778780781445676E-14 ) ) ;
#2965=DIRECTION ( 'NONE',  ( 1.000000000000000000, 0.000000000000000000, 0.000000000000000000 ) ) ;
#3025=DIRECTION ( 'NONE',  ( 0.000000000000000000, -5.551115123125748189E-17, -1.000000000000000000 ) ) ;
#3037=ORIENTED_EDGE ( 'NONE', *, *, #17681, .F. ) ;
#3041=VECTOR ( 'NONE', #497, 1000.000000000000000 ) ;
#3067=( NAMED_UNIT ( * ) PLANE_ANGLE_UNIT ( ) SI_UNIT ( $, .RADIAN. ) );
#3072=CARTESIAN_POINT ( 'NONE',  ( 0.000000000000000000, 0.000000000000000000, 0.000000000000000000 ) ) ;
#3076=ADVANCED_FACE ( 'NONE', ( #9957 ), #11719, .T. ) ;
#3170=CARTESIAN_POINT ( 'NONE',  ( 5.299999999999998934, 0.000000000000000000, 0.000000000000000000 ) ) ;
#3215=DIRECTION ( 'NONE',  ( 1.000000000000000000, 0.000000000000000000, 0.000000000000000000 ) ) ;
#3219=EDGE_CURVE ( 'NONE', #15837, #17074, #7017, .T. ) ;
#3226=CARTESIAN_POINT ( 'NONE',  ( 0.05458999538772711657, -1.264741368073410532, 6.499999999999984013 ) ) ;
#3231=DIRECTION ( 'NONE',  ( 1.000000000000000000, 0.000000000000000000, 0.000000000000000000 ) ) ;
#3246=DIRECTION ( 'NONE',  ( 0.000000000000000000, 5.551115123125747573E-17, 1.000000000000000000 ) ) ;
#3265=CARTESIAN_POINT ( 'NONE',  ( 0.000000000000000000, 0.000000000000000000, 0.000000000000000000 ) ) ;
#3270=DIRECTION ( 'NONE',  ( 1.000000000000000000, 0.000000000000000000, 0.000000000000000000 ) ) ;
#3391=ORIENTED_EDGE ( 'NONE', *, *, #9855, .T. ) ;
#3409=VECTOR ( 'NONE', #16033, 1000.000000000000000 ) ;
#3415=EDGE_LOOP ( 'NONE', ( #2438, #5937, #17018 ) ) ;
#3462=FACE_OUTER_BOUND ( 'NONE', #7288, .T. ) ;
#3471=ORIENTED_EDGE ( 'NONE', *, *, #6167, .F. ) ;
#3491=PRODUCT_DEFINITION ( 'UNKNOWN', '', #14165, #7047 ) ;
#3538=LINE ( 'NONE', #11963, #9954 ) ;
#3553=VERTEX_POINT ( 'NONE', #18496 ) ;
#3554=EDGE_CURVE ( 'NONE', #17364, #16487, #11014, .T. ) ;
#3556=ADVANCED_FACE ( 'NONE', ( #5665 ), #9599, .F. ) ;
#3594=ORIENTED_EDGE ( 'NONE', *, *, #15888, .F. ) ;
#3613=DIRECTION ( 'NONE',  ( 0.000000000000000000, 5.551115123125747573E-17, 1.000000000000000000 ) ) ;
#3619=ORIENTED_EDGE ( 'NONE', *, *, #6157, .F. ) ;
#3731=ORIENTED_EDGE ( 'NONE', *, *, #11294, .F. ) ;
#3792=PLANE ( 'NONE',  #747 ) ;
#3814=DIRECTION ( 'NONE',  ( -1.000000000000000000, 0.000000000000000000, 0.000000000000000000 ) ) ;
#3827=CARTESIAN_POINT ( 'NONE',  ( 5.299999999999998934, 0.000000000000000000, 0.000000000000000000 ) ) ;
#3847=B_SPLINE_CURVE_WITH_KNOTS ( 'NONE', 3,
 ( #5520, #5318, #2528, #9532, #1036, #6922, #12649, #15522 ),
 .UNSPECIFIED., .F., .F.,
 ( 4, 2, 2, 4 ),
 ( 0.003797433802554399471, 0.004743183970586228350, 0.005688934138618056795, 0.007580434474681712817 ),
 .UNSPECIFIED. ) ;
#3851=DIRECTION ( 'NONE',  ( -1.000000000000000000, 0.000000000000000000, 0.000000000000000000 ) ) ;
#3884=AXIS2_PLACEMENT_3D ( 'NONE', #12392, #2352, #18175 ) ;
#3914=CARTESIAN_POINT ( 'NONE',  ( 8.065334786029138841E-14, -5.788408252968062051, -2.974182810908597041 ) ) ;
#3917=FACE_OUTER_BOUND ( 'NONE', #6327, .T. ) ;
#3942=DIRECTION ( 'NONE',  ( 0.000000000000000000, 0.4999999999999999445, -0.8660254037844387076 ) ) ;
#3985=DIRECTION ( 'NONE',  ( -1.000000000000000000, 0.000000000000000000, 0.000000000000000000 ) ) ;
#3988=CIRCLE ( 'NONE', #13851, 4.400000000000027889 ) ;
#4056=ADVANCED_FACE ( 'NONE', ( #15680 ), #8357, .T. ) ;
#4059=DIRECTION ( 'NONE',  ( 0.000000000000000000, -0.8660254037844381525, -0.5000000000000008882 ) ) ;
#4090=DIRECTION ( 'NONE',  ( -1.000000000000000000, 0.000000000000000000, 0.000000000000000000 ) ) ;
#4125=DIRECTION ( 'NONE',  ( 1.000000000000000000, 0.000000000000000000, 0.000000000000000000 ) ) ;
#4168=CARTESIAN_POINT ( 'NONE',  ( 5.299999999999998934, 7.505553499465141165, -1.387778780781445676E-14 ) ) ;
#4186=CARTESIAN_POINT ( 'NONE',  ( 0.5805565836007609004, -3.752776749732712691, -6.500000000000033751 ) ) ;
#4201=CARTESIAN_POINT ( 'NONE',  ( 0.000000000000000000, 0.000000000000000000, 0.000000000000000000 ) ) ;
#4210=VERTEX_POINT ( 'NONE', #13600 ) ;
#4218=ORIENTED_EDGE ( 'NONE', *, *, #6157, .T. ) ;
#4273=ADVANCED_FACE ( 'NONE', ( #15268 ), #11648, .T. ) ;
#4283=AXIS2_PLACEMENT_3D ( 'NONE', #11034, #16719, #5411 ) ;
#4318=LINE ( 'NONE', #12935, #4614 ) ;
#4319=CARTESIAN_POINT ( 'NONE',  ( 0.06682554136344981410, -4.993536075455556222, 4.350941807883138779 ) ) ;
#4343=CIRCLE ( 'NONE', #16877, 6.500000000000039968 ) ;
#4375=VERTEX_POINT ( 'NONE', #12853 ) ;
#4416=ORIENTED_EDGE ( 'NONE', *, *, #9855, .F. ) ;
#4428=CARTESIAN_POINT ( 'NONE',  ( 0.000000000000000000, 0.000000000000000000, 0.000000000000000000 ) ) ;
#4453=CARTESIAN_POINT ( 'NONE',  ( 0.5805565836007609004, 3.752776749732435135, 6.499999999999981348 ) ) ;
#4462=( LENGTH_UNIT ( ) NAMED_UNIT ( * ) SI_UNIT ( .MILLI., .METRE. ) );
#4469=CYLINDRICAL_SURFACE ( 'NONE', #16575, 6.500000000000039968 ) ;
#4478=B_SPLINE_CURVE_WITH_KNOTS ( 'NONE', 3,
 ( #15994, #17299, #5887, #10378, #8892, #14587 ),
 .UNSPECIFIED., .F., .F.,
 ( 4, 2, 4 ),
 ( 2.380733003268861808E-07, 0.001898835937927363139, 0.003797433802554399471 ),
 .UNSPECIFIED. ) ;
#4503=AXIS2_PLACEMENT_3D ( 'NONE', #10338, #3215, #16813 ) ;
#4504=VECTOR ( 'NONE', #17919, 1000.000000000000000 ) ;
#4531=CARTESIAN_POINT ( 'NONE',  ( 0.2565376335216263959, -2.516992571280132651, 6.499999999999984013 ) ) ;
#4539=VECTOR ( 'NONE', #8791, 1000.000000000000000 ) ;
#4614=VECTOR ( 'NONE', #10031, 999.9999999999998863 ) ;
#4622=AXIS2_PLACEMENT_3D ( 'NONE', #13944, #6534, #1037 ) ;
#4625=ORIENTED_EDGE ( 'NONE', *, *, #18094, .T. ) ;
#4760=DIRECTION ( 'NONE',  ( 1.000000000000000000, 0.000000000000000000, 0.000000000000000000 ) ) ;
#4796=EDGE_LOOP ( 'NONE', ( #12549, #5812 ) ) ;
#4821=ORIENTED_EDGE ( 'NONE', *, *, #10984, .F. ) ;
#4832=DIRECTION ( 'NONE',  ( -1.000000000000000000, 0.000000000000000000, 0.000000000000000000 ) ) ;
#4848=DIRECTION ( 'NONE',  ( -1.000000000000000000, 0.000000000000000000, 0.000000000000000000 ) ) ;
#4852=CARTESIAN_POINT ( 'NONE',  ( 5.699999999999996625, 2.220446049250299276E-16, 4.000000000000000000 ) ) ;
#4869=CIRCLE ( 'NONE', #7281, 0.4000000000000001887 ) ;
#4912=ADVANCED_FACE ( 'NONE', ( #6927 ), #18446, .F. ) ;
#4955=CARTESIAN_POINT ( 'NONE',  ( 0.000000000000000000, 5.629165124598635828, -3.250000000000016875 ) ) ;
#4995=CYLINDRICAL_SURFACE ( 'NONE', #5816, 4.000000000000024869 ) ;
#5016=LINE ( 'NONE', #10936, #11786 ) ;
#5054=DIRECTION ( 'NONE',  ( 1.000000000000000000, 0.000000000000000000, 0.000000000000000000 ) ) ;
#5074=ORIENTED_EDGE ( 'NONE', *, *, #2628, .F. ) ;
#5120=AXIS2_PLACEMENT_3D ( 'NONE', #11804, #3270, #6245 ) ;
#5166=ADVANCED_FACE ( 'NONE', ( #5400 ), #11682, .T. ) ;
#5213=ORIENTED_EDGE ( 'NONE', *, *, #1402, .F. ) ;
#5230=CARTESIAN_POINT ( 'NONE',  ( 5.699999999999996625, 0.000000000000000000, 0.000000000000000000 ) ) ;
#5232=DIRECTION ( 'NONE',  ( 1.000000000000000000, 0.000000000000000000, 0.000000000000000000 ) ) ;
#5302=FACE_OUTER_BOUND ( 'NONE', #12758, .T. ) ;
#5312=ORIENTED_EDGE ( 'NONE', *, *, #17681, .T. ) ;
#5314=DIRECTION ( 'NONE',  ( 0.000000000000000000, -5.551115123125747573E-17, -1.000000000000000000 ) ) ;
#5316=DIRECTION ( 'NONE',  ( 0.000000000000000000, -1.000000000000000000, 5.551115123125748189E-17 ) ) ;
#5318=CARTESIAN_POINT ( 'NONE',  ( -8.273817828780008867E-15, 5.788408252967876422, 2.974182810908626351 ) ) ;
#5343=CARTESIAN_POINT ( 'NONE',  ( 0.5805565836007609004, 7.505553499465141165, -1.387778780781445676E-14 ) ) ;
#5355=SHAPE_DEFINITION_REPRESENTATION ( #11205, #5501 ) ;
#5400=FACE_OUTER_BOUND ( 'NONE', #7718, .T. ) ;
#5411=DIRECTION ( 'NONE',  ( 0.000000000000000000, -0.5000000000000008882, -0.8660254037844381525 ) ) ;
#5439=DIRECTION ( 'NONE',  ( -1.000000000000000000, 0.000000000000000000, 0.000000000000000000 ) ) ;
#5444=CIRCLE ( 'NONE', #15898, 6.500000000000039968 ) ;
#5497=( GEOMETRIC_REPRESENTATION_CONTEXT ( 3 ) GLOBAL_UNCERTAINTY_ASSIGNED_CONTEXT ( ( #2550 ) ) GLOBAL_UNIT_ASSIGNED_CONTEXT ( ( #13330, #1723, #9026 ) ) REPRESENTATION_CONTEXT ( 'NONE', 'WORKASPACE' ) );
#5501=SHAPE_REPRESENTATION ( 'hex bolt gradeab fine_iso_ISO 8765 - M8x1.0 x 40 x 22-N', ( #16217 ), #15033 ) ;
#5520=CARTESIAN_POINT ( 'NONE',  ( 0.000000000000000000, 5.629165124598801917, 3.250000000000037748 ) ) ;
#5546=AXIS2_PLACEMENT_3D ( 'NONE', #15523, #8424, #15884 ) ;
#5547=CIRCLE ( 'NONE', #12113, 6.500000000000039968 ) ;
#5585=CARTESIAN_POINT ( 'NONE',  ( 5.299999999999998934, 4.351979364426058414E-16, -6.499999999999999112 ) ) ;
#5591=DIRECTION ( 'NONE',  ( -1.000000000000000000, 0.000000000000000000, 0.000000000000000000 ) ) ;
#5608=B_SPLINE_CURVE_WITH_KNOTS ( 'NONE', 3,
 ( #18513, #3914, #1211, #11031, #2808, #11133, #14125, #17007 ),
 .UNSPECIFIED., .F., .F.,
 ( 4, 2, 2, 4 ),
 ( 0.003797433802554432431, 0.004743183970586246564, 0.005688934138618060264, 0.007580434474681690266 ),
 .UNSPECIFIED. ) ;
#5642=AXIS2_PLACEMENT_3D ( 'NONE', #11887, #4760, #16281 ) ;
#5663=ORIENTED_EDGE ( 'NONE', *, *, #9799, .T. ) ;
#5665=FACE_OUTER_BOUND ( 'NONE', #9450, .T. ) ;
#5680=ORIENTED_EDGE ( 'NONE', *, *, #8605, .F. ) ;
#5710=ADVANCED_FACE ( 'NONE', ( #16010 ), #14016, .T. ) ;
#5738=AXIS2_PLACEMENT_3D ( 'NONE', #11860, #4832, #2369 ) ;
#5753=CIRCLE ( 'NONE', #15915, 6.500000000000039968 ) ;
#5781=CARTESIAN_POINT ( 'NONE',  ( 0.000000000000000000, 0.000000000000000000, 0.000000000000000000 ) ) ;
#5785=CARTESIAN_POINT ( 'NONE',  ( 45.30000000000000426, 2.492512489064173907E-16, -3.445500000000000451 ) ) ;
#5807=LINE ( 'NONE', #15458, #15532 ) ;
#5811=CARTESIAN_POINT ( 'NONE',  ( 5.299999999999998934, 7.505553499465141165, -1.387778780781445676E-14 ) ) ;
#5812=ORIENTED_EDGE ( 'NONE', *, *, #10984, .T. ) ;
#5816=AXIS2_PLACEMENT_3D ( 'NONE', #14823, #6490, #13427 ) ;
#5826=CARTESIAN_POINT ( 'NONE',  ( 0.000000000000000000, 5.629165124598801917, 3.250000000000037748 ) ) ;
#5874=DIRECTION ( 'NONE',  ( 0.000000000000000000, 5.551115123125748189E-17, 1.000000000000000000 ) ) ;
#5887=CARTESIAN_POINT ( 'NONE',  ( 0.2573354458087894203, 4.368923434677159712, 5.432802636760818871 ) ) ;
#5892=ORIENTED_EDGE ( 'NONE', *, *, #13149, .T. ) ;
#5937=ORIENTED_EDGE ( 'NONE', *, *, #11294, .T. ) ;
#5963=VERTEX_POINT ( 'NONE', #7209 ) ;
#5998=CARTESIAN_POINT ( 'NONE',  ( 0.05533025579370332708, -6.264553569211981809, 2.149474931388166699 ) ) ;
#6031=EDGE_LOOP ( 'NONE', ( #9202, #1331 ) ) ;
#6037=DIRECTION ( 'NONE',  ( 0.000000000000000000, 0.000000000000000000, 1.000000000000000000 ) ) ;
#6054=CIRCLE ( 'NONE', #15927, 0.4000000000000001887 ) ;
#6064=CARTESIAN_POINT ( 'NONE',  ( 0.000000000000000000, -5.629165124598954684, 3.250000000000013323 ) ) ;
#6074=LINE ( 'NONE', #8817, #17955 ) ;
#6157=EDGE_CURVE ( 'NONE', #15640, #10340, #13456, .T. ) ;
#6167=EDGE_CURVE ( 'NONE', #4375, #7124, #10657, .T. ) ;
#6245=DIRECTION ( 'NONE',  ( 0.000000000000000000, -5.551115123125747573E-17, -1.000000000000000000 ) ) ;
#6258=EDGE_CURVE ( 'NONE', #10059, #1357, #8596, .T. ) ;
#6311=AXIS2_PLACEMENT_3D ( 'NONE', #18502, #2965, #10080 ) ;
#6327=EDGE_LOOP ( 'NONE', ( #9231, #14767, #4625 ) ) ;
#6344=ORIENTED_EDGE ( 'NONE', *, *, #16092, .T. ) ;
#6354=ORIENTED_EDGE ( 'NONE', *, *, #1285, .T. ) ;
#6370=CARTESIAN_POINT ( 'NONE',  ( 0.05458999538779253646, -1.264741368073575511, -6.500000000000063949 ) ) ;
#6422=DIRECTION ( 'NONE',  ( -1.000000000000000000, 0.000000000000000000, 0.000000000000000000 ) ) ;
#6426=VECTOR ( 'NONE', #12436, 1000.000000000000000 ) ;
#6468=CARTESIAN_POINT ( 'NONE',  ( 5.303146227817084385E-14, -0.6346842323190391433, -6.500000000000061284 ) ) ;
#6483=CARTESIAN_POINT ( 'NONE',  ( 0.000000000000000000, 7.505553499465141165, -1.387778780781445676E-14 ) ) ;
#6490=DIRECTION ( 'NONE',  ( -1.000000000000000000, 0.000000000000000000, 0.000000000000000000 ) ) ;
#6517=ORIENTED_EDGE ( 'NONE', *, *, #6167, .T. ) ;
#6531=DIRECTION ( 'NONE',  ( 0.000000000000000000, -5.551115123125748189E-17, -1.000000000000000000 ) ) ;
#6534=DIRECTION ( 'NONE',  ( 1.000000000000000000, 0.000000000000000000, 0.000000000000000000 ) ) ;
#6557=CARTESIAN_POINT ( 'NONE',  ( 0.000000000000000000, 0.000000000000000000, 0.000000000000000000 ) ) ;
#6609=FACE_OUTER_BOUND ( 'NONE', #6793, .T. ) ;
#6666=VERTEX_POINT ( 'NONE', #16022 ) ;
#6670=CIRCLE ( 'NONE', #997, 4.000000000000024869 ) ;
#6681=PRODUCT_CONTEXT ( 'NONE', #17202, 'mechanical' ) ;
#6691=DIRECTION ( 'NONE',  ( -1.000000000000000000, 0.000000000000000000, 0.000000000000000000 ) ) ;
#6732=FACE_OUTER_BOUND ( 'NONE', #11099, .T. ) ;
#6742=EDGE_CURVE ( 'NONE', #7250, #18326, #7167, .T. ) ;
#6793=EDGE_LOOP ( 'NONE', ( #8269, #16846, #14285 ) ) ;
#6796=DIRECTION ( 'NONE',  ( 1.000000000000000000, 0.000000000000000000, 0.000000000000000000 ) ) ;
#6854=ORIENTED_EDGE ( 'NONE', *, *, #11891, .F. ) ;
#6874=ORIENTED_EDGE ( 'NONE', *, *, #1402, .T. ) ;
#6884=ADVANCED_FACE ( 'NONE', ( #7878 ), #13774, .T. ) ;
#6893=DIRECTION ( 'NONE',  ( 0.000000000000000000, 0.8660254037844387076, 0.4999999999999999445 ) ) ;
#6922=CARTESIAN_POINT ( 'NONE',  ( 0.2578475836320668346, 6.890627091270365767, 1.065083781909175187 ) ) ;
#6927=FACE_OUTER_BOUND ( 'NONE', #11643, .T. ) ;
#6929=AXIS2_PLACEMENT_3D ( 'NONE', #6557, #5439, #10777 ) ;
#6932=EDGE_LOOP ( 'NONE', ( #14224, #6874 ) ) ;
#6941=B_SPLINE_CURVE_WITH_KNOTS ( 'NONE', 3,
 ( #8567, #7073, #7414, #5998, #11726, #8918 ),
 .UNSPECIFIED., .F., .F.,
 ( 4, 2, 4 ),
 ( 2.380733003239153451E-07, 0.001898835937927371162, 0.003797433802554418120 ),
 .UNSPECIFIED. ) ;
#6944=CARTESIAN_POINT ( 'NONE',  ( 0.5805565836007609004, 3.752776749732559924, -6.500000000000061284 ) ) ;
#6997=ADVANCED_FACE ( 'NONE', ( #2644 ), #18371, .F. ) ;
#7013=CIRCLE ( 'NONE', #124, 6.500000000000039968 ) ;
#7017=CIRCLE ( 'NONE', #12072, 3.445500000000021767 ) ;
#7047=PRODUCT_DEFINITION_CONTEXT ( 'detailed design', #2022, 'design' ) ;
#7073=CARTESIAN_POINT ( 'NONE',  ( 0.4033376246893360939, -7.198601258567047800, 0.5316568767328908596 ) ) ;
#7115=FACE_OUTER_BOUND ( 'NONE', #16644, .T. ) ;
#7124=VERTEX_POINT ( 'NONE', #479 ) ;
#7125=ADVANCED_FACE ( 'NONE', ( #6609 ), #9311, .T. ) ;
#7126=EDGE_CURVE ( 'NONE', #9885, #15640, #6074, .T. ) ;
#7143=ORIENTED_EDGE ( 'NONE', *, *, #15921, .F. ) ;
#7167=B_SPLINE_CURVE_WITH_KNOTS ( 'NONE', 3,
 ( #8917, #12098, #7692, #7785, #10492, #16095 ),
 .UNSPECIFIED., .F., .F.,
 ( 4, 2, 4 ),
 ( 2.380733003370977718E-07, 0.001898835937927384606, 0.003797433802554432431 ),
 .UNSPECIFIED. ) ;
#7179=ORIENTED_EDGE ( 'NONE', *, *, #16889, .T. ) ;
#7194=DIRECTION ( 'NONE',  ( 1.000000000000000000, 0.000000000000000000, 0.000000000000000000 ) ) ;
#7200=CARTESIAN_POINT ( 'NONE',  ( 4.699999999999995737, 3.752776749732559924, -6.500000000000061284 ) ) ;
#7205=CIRCLE ( 'NONE', #16134, 4.000000000000024869 ) ;
#7209=CARTESIAN_POINT ( 'NONE',  ( 44.74549999999999272, 2.220446049250313081E-16, 4.000000000000024869 ) ) ;
#7250=VERTEX_POINT ( 'NONE', #4186 ) ;
#7276=B_SPLINE_CURVE_WITH_KNOTS ( 'NONE', 3,
 ( #1340, #12842, #6, #4319, #7393, #8717, #17300, #15905 ),
 .UNSPECIFIED., .F., .F.,
 ( 4, 2, 2, 4 ),
 ( 0.003797433802554418120, 0.004743183970586237024, 0.005688934138618055927, 0.007580434474681694602 ),
 .UNSPECIFIED. ) ;
#7281=AXIS2_PLACEMENT_3D ( 'NONE', #8028, #5316, #12164 ) ;
#7288=EDGE_LOOP ( 'NONE', ( #8021, #8828, #11090, #756 ) ) ;
#7291=DIRECTION ( 'NONE',  ( 0.000000000000000000, 5.551115123125747573E-17, 1.000000000000000000 ) ) ;
#7293=CARTESIAN_POINT ( 'NONE',  ( 0.000000000000000000, -4.857225732735059864E-14, 6.500000000000037303 ) ) ;
#7308=AXIS2_PLACEMENT_3D ( 'NONE', #9304, #2365, #12409 ) ;
#7327=ORIENTED_EDGE ( 'NONE', *, *, #8605, .T. ) ;
#7331=ADVANCED_FACE ( 'NONE', ( #8863 ), #11752, .T. ) ;
#7354=VERTEX_POINT ( 'NONE', #8772 ) ;
#7363=CARTESIAN_POINT ( 'NONE',  ( 0.000000000000000000, 3.608224830031758263E-16, 6.500000000000039968 ) ) ;
#7377=ORIENTED_EDGE ( 'NONE', *, *, #9740, .T. ) ;
#7381=CARTESIAN_POINT ( 'NONE',  ( 0.4053525175236455391, 3.145852061456137161, 6.499999999999982236 ) ) ;
#7393=CARTESIAN_POINT ( 'NONE',  ( 0.1061556211656023985, -4.836380039389555741, 4.623144047065584239 ) ) ;
#7414=CARTESIAN_POINT ( 'NONE',  ( 0.2573354458088682462, -6.889406814520657285, 1.067197363239251295 ) ) ;
#7417=ORIENTED_EDGE ( 'NONE', *, *, #10999, .F. ) ;
#7485=PLANE ( 'NONE',  #17369 ) ;
#7522=LINE ( 'NONE', #17252, #13866 ) ;
#7528=CARTESIAN_POINT ( 'NONE',  ( 0.4042117618284869485, -3.141900367810146921, 6.499999999999983125 ) ) ;
#7536=CIRCLE ( 'NONE', #12947, 6.500000000000039968 ) ;
#7590=VERTEX_POINT ( 'NONE', #13693 ) ;
#7623=CARTESIAN_POINT ( 'NONE',  ( 4.699999999999995737, 7.505553499465141165, -1.387778780781445676E-14 ) ) ;
#7667=CARTESIAN_POINT ( 'NONE',  ( 0.000000000000000000, -5.629165124598996428, -3.250000000000020428 ) ) ;
#7688=ORIENTED_EDGE ( 'NONE', *, *, #6258, .T. ) ;
#7692=CARTESIAN_POINT ( 'NONE',  ( 0.2573354458088474295, -4.368923434677343565, -5.432802636760800219 ) ) ;
#7718=EDGE_LOOP ( 'NONE', ( #7915, #13390, #3594 ) ) ;
#7734=DIRECTION ( 'NONE',  ( -1.000000000000000000, 0.000000000000000000, 0.000000000000000000 ) ) ;
#7768=ORIENTED_EDGE ( 'NONE', *, *, #2250, .F. ) ;
#7781=ORIENTED_EDGE ( 'NONE', *, *, #9740, .F. ) ;
#7785=CARTESIAN_POINT ( 'NONE',  ( 0.05533025579369500735, -4.993776679986010159, -4.350525068611887036 ) ) ;
#7823=DIRECTION ( 'NONE',  ( 1.000000000000000000, 0.000000000000000000, 0.000000000000000000 ) ) ;
#7833=ORIENTED_EDGE ( 'NONE', *, *, #7126, .T. ) ;
#7875=CARTESIAN_POINT ( 'NONE',  ( 0.000000000000000000, 5.629165124598635828, -3.250000000000016875 ) ) ;
#7878=FACE_OUTER_BOUND ( 'NONE', #14463, .T. ) ;
#7896=ADVANCED_FACE ( 'NONE', ( #1442 ), #16795, .T. ) ;
#7905=CARTESIAN_POINT ( 'NONE',  ( 4.699999999999995737, -2.914335439641035919E-13, -6.500000000000019540 ) ) ;
#7915=ORIENTED_EDGE ( 'NONE', *, *, #9750, .T. ) ;
#7922=ORIENTED_EDGE ( 'NONE', *, *, #10903, .F. ) ;
#7959=ORIENTED_EDGE ( 'NONE', *, *, #17032, .F. ) ;
#7975=VERTEX_POINT ( 'NONE', #5826 ) ;
#7991=FACE_OUTER_BOUND ( 'NONE', #2353, .T. ) ;
#8017=ORIENTED_EDGE ( 'NONE', *, *, #1415, .F. ) ;
#8021=ORIENTED_EDGE ( 'NONE', *, *, #2571, .F. ) ;
#8028=CARTESIAN_POINT ( 'NONE',  ( 5.699999999999996625, -2.442490654175344586E-16, -4.400000000000027889 ) ) ;
#8055=LINE ( 'NONE', #9557, #2138 ) ;
#8058=CARTESIAN_POINT ( 'NONE',  ( 0.000000000000000000, -2.914335439641035919E-13, -6.500000000000019540 ) ) ;
#8104=ADVANCED_FACE ( 'NONE', ( #17508 ), #17406, .T. ) ;
#8133=FACE_OUTER_BOUND ( 'NONE', #14586, .T. ) ;
#8138=CARTESIAN_POINT ( 'NONE',  ( 4.699999999999995737, -4.857225732735059864E-14, 6.500000000000037303 ) ) ;
#8188=DIRECTION ( 'NONE',  ( 0.000000000000000000, 5.551115123125747573E-17, 1.000000000000000000 ) ) ;
#8231=PLANE ( 'NONE',  #12059 ) ;
#8269=ORIENTED_EDGE ( 'NONE', *, *, #9149, .T. ) ;
#8294=DIRECTION ( 'NONE',  ( 0.000000000000000000, -5.551115123125747573E-17, -1.000000000000000000 ) ) ;
#8328=FACE_OUTER_BOUND ( 'NONE', #9364, .T. ) ;
#8340=DIRECTION ( 'NONE',  ( 0.000000000000000000, 5.551115123125748189E-17, 1.000000000000000000 ) ) ;
#8343=FACE_OUTER_BOUND ( 'NONE', #1940, .T. ) ;
#8357=CONICAL_SURFACE ( 'NONE', #283, 6.500000000000039968, 1.047197551196600296 ) ;
#8388=DIRECTION ( 'NONE',  ( -0.7071067811865496822, 4.734329415645505418E-17, -0.7071067811865453523 ) ) ;
#8391=PLANE ( 'NONE',  #13553 ) ;
#8393=AXIS2_PLACEMENT_3D ( 'NONE', #16994, #9710, #11018 ) ;
#8424=DIRECTION ( 'NONE',  ( 0.000000000000000000, 0.8660254037844375974, -0.5000000000000017764 ) ) ;
#8431=PLANE ( 'NONE',  #12577 ) ;
#8467=EDGE_LOOP ( 'NONE', ( #5213, #15776, #7922, #11417, #3037, #6854 ) ) ;
#8534=ORIENTED_EDGE ( 'NONE', *, *, #1285, .F. ) ;
#8567=CARTESIAN_POINT ( 'NONE',  ( 0.5805565836007747782, -7.505553499465293932, 1.040834085586084257E-14 ) ) ;
#8578=DIRECTION ( 'NONE',  ( 0.000000000000000000, -0.5000000000000017764, -0.8660254037844377084 ) ) ;
#8596=LINE ( 'NONE', #11229, #23 ) ;
#8605=EDGE_CURVE ( 'NONE', #10059, #5963, #6670, .T. ) ;
#8611=CARTESIAN_POINT ( 'NONE',  ( 0.2595206531158220642, 2.531175536751704147, 6.499999999999982236 ) ) ;
#8632=ORIENTED_EDGE ( 'NONE', *, *, #17911, .F. ) ;
#8717=CARTESIAN_POINT ( 'NONE',  ( 0.2578475836321327264, -4.367703157927462776, 5.434916218090863893 ) ) ;
#8765=LINE ( 'NONE', #7363, #1635 ) ;
#8772=CARTESIAN_POINT ( 'NONE',  ( 4.699999999999995737, 5.629165124598801917, 3.250000000000037748 ) ) ;
#8781=CIRCLE ( 'NONE', #12684, 4.000000000000024869 ) ;
#8788=CARTESIAN_POINT ( 'NONE',  ( 4.699999999999995737, -7.505553499465293932, 1.040834085586084257E-14 ) ) ;
#8790=FACE_OUTER_BOUND ( 'NONE', #8467, .T. ) ;
#8791=DIRECTION ( 'NONE',  ( -0.7071067811865496822, 3.925231146709400939E-17, 0.7071067811865453523 ) ) ;
#8817=CARTESIAN_POINT ( 'NONE',  ( 4.699999999999995737, 3.752776749732559924, -6.500000000000061284 ) ) ;
#8828=ORIENTED_EDGE ( 'NONE', *, *, #10411, .T. ) ;
#8863=FACE_OUTER_BOUND ( 'NONE', #16055, .T. ) ;
#8879=DIRECTION ( 'NONE',  ( -1.000000000000000000, 0.000000000000000000, 0.000000000000000000 ) ) ;
#8881=DIRECTION ( 'NONE',  ( -1.000000000000000000, -0.000000000000000000, -0.000000000000000000 ) ) ;
#8892=CARTESIAN_POINT ( 'NONE',  ( -3.887881227897240134E-15, 5.309483803148766334, 3.803704290982293124 ) ) ;
#8917=CARTESIAN_POINT ( 'NONE',  ( 0.5805565836007609004, -3.752776749732712691, -6.500000000000033751 ) ) ;
#8918=CARTESIAN_POINT ( 'NONE',  ( 0.000000000000000000, -5.629165124598954684, 3.250000000000013323 ) ) ;
#8924=EDGE_CURVE ( 'NONE', #17074, #15837, #9906, .T. ) ;
#8947=VERTEX_POINT ( 'NONE', #9574 ) ;
#8961=DIRECTION ( 'NONE',  ( 1.000000000000000000, 0.000000000000000000, 0.000000000000000000 ) ) ;
#8988=DIRECTION ( 'NONE',  ( 0.000000000000000000, -5.551115123125748806E-17, -1.000000000000000000 ) ) ;
#9026=( NAMED_UNIT ( * ) SI_UNIT ( $, .STERADIAN. ) SOLID_ANGLE_UNIT ( ) );
#9028=VERTEX_POINT ( 'NONE', #14269 ) ;
#9063=EDGE_CURVE ( 'NONE', #10340, #12345, #17233, .T. ) ;
#9097=EDGE_LOOP ( 'NONE', ( #13734, #9672, #7143, #18336 ) ) ;
#9103=CARTESIAN_POINT ( 'NONE',  ( 0.05533025579362768620, 6.264553569211829043, -2.149474931388220433 ) ) ;
#9124=DIRECTION ( 'NONE',  ( -1.000000000000000000, 0.000000000000000000, 0.000000000000000000 ) ) ;
#9125=ORIENTED_EDGE ( 'NONE', *, *, #14808, .T. ) ;
#9149=EDGE_CURVE ( 'NONE', #12345, #7124, #18142, .T. ) ;
#9175=CARTESIAN_POINT ( 'NONE',  ( 4.699999999999995737, 7.505553499465141165, -1.387778780781445676E-14 ) ) ;
#9192=VERTEX_POINT ( 'NONE', #2734 ) ;
#9202=ORIENTED_EDGE ( 'NONE', *, *, #8924, .F. ) ;
#9231=ORIENTED_EDGE ( 'NONE', *, *, #11802, .T. ) ;
#9232=LINE ( 'NONE', #14747, #4504 ) ;
#9261=ADVANCED_FACE ( 'NONE', ( #8343 ), #7485, .F. ) ;
#9283=CARTESIAN_POINT ( 'NONE',  ( 0.000000000000000000, 5.629165124598635828, -3.250000000000016875 ) ) ;
#9304=CARTESIAN_POINT ( 'NONE',  ( 0.000000000000000000, 0.000000000000000000, 0.000000000000000000 ) ) ;
#9311=CONICAL_SURFACE ( 'NONE', #5120, 6.500000000000039968, 1.047197551196600296 ) ;
#9364=EDGE_LOOP ( 'NONE', ( #7833, #5892, #602 ) ) ;
#9367=CIRCLE ( 'NONE', #110, 6.500000000000039968 ) ;
#9374=CARTESIAN_POINT ( 'NONE',  ( 0.5805565836007609004, 7.505553499465141165, -1.387778780781445676E-14 ) ) ;
#9386=VECTOR ( 'NONE', #15602, 999.9999999999998863 ) ;
#9450=EDGE_LOOP ( 'NONE', ( #18177, #7179, #7768, #12465, #2275, #14563 ) ) ;
#9481=DIRECTION ( 'NONE',  ( 0.000000000000000000, 5.551115123125748189E-17, 1.000000000000000000 ) ) ;
#9495=ORIENTED_EDGE ( 'NONE', *, *, #14808, .F. ) ;
#9532=CARTESIAN_POINT ( 'NONE',  ( 0.06682554136337354178, 6.264794173742258998, 2.149058192116914068 ) ) ;
#9557=CARTESIAN_POINT ( 'NONE',  ( 0.000000000000000000, 2.220446049250313081E-16, 4.000000000000024869 ) ) ;
#9574=CARTESIAN_POINT ( 'NONE',  ( 4.699999999999995737, -5.629165124598954684, 3.250000000000013323 ) ) ;
#9582=VERTEX_POINT ( 'NONE', #14134 ) ;
#9599=PLANE ( 'NONE',  #10431 ) ;
#9636=ORIENTED_EDGE ( 'NONE', *, *, #820, .F. ) ;
#9672=ORIENTED_EDGE ( 'NONE', *, *, #2, .T. ) ;
#9710=DIRECTION ( 'NONE',  ( 1.000000000000000000, 0.000000000000000000, 0.000000000000000000 ) ) ;
#9740=EDGE_CURVE ( 'NONE', #850, #18326, #15295, .T. ) ;
#9742=EDGE_CURVE ( 'NONE', #17074, #5963, #1675, .T. ) ;
#9750=EDGE_CURVE ( 'NONE', #9582, #14582, #941, .T. ) ;
#9752=ORIENTED_EDGE ( 'NONE', *, *, #15764, .F. ) ;
#9790=ORIENTED_EDGE ( 'NONE', *, *, #15888, .T. ) ;
#9799=EDGE_CURVE ( 'NONE', #3553, #16487, #16847, .T. ) ;
#9821=CARTESIAN_POINT ( 'NONE',  ( 0.5805565836007609004, 3.752776749732559924, -6.500000000000061284 ) ) ;
#9823=DIRECTION ( 'NONE',  ( -1.000000000000000000, 0.000000000000000000, 0.000000000000000000 ) ) ;
#9829=CARTESIAN_POINT ( 'NONE',  ( 4.699999999999995737, 6.499999999999901412, 2.428612866367529932E-14 ) ) ;
#9831=ORIENTED_EDGE ( 'NONE', *, *, #9750, .F. ) ;
#9842=CARTESIAN_POINT ( 'NONE',  ( 0.2578475836320997527, 4.367703157927319779, -5.434916218090905637 ) ) ;
#9855=EDGE_CURVE ( 'NONE', #16487, #11023, #13806, .T. ) ;
#9857=ORIENTED_EDGE ( 'NONE', *, *, #2571, .T. ) ;
#9885=VERTEX_POINT ( 'NONE', #453 ) ;
#9891=DIRECTION ( 'NONE',  ( 0.000000000000000000, -0.4999999999999999445, 0.8660254037844387076 ) ) ;
#9906=CIRCLE ( 'NONE', #2425, 3.445500000000021767 ) ;
#9916=CARTESIAN_POINT ( 'NONE',  ( 0.000000000000000000, 0.000000000000000000, 0.000000000000000000 ) ) ;
#9922=PLANE ( 'NONE',  #5546 ) ;
#9939=FACE_OUTER_BOUND ( 'NONE', #1248, .T. ) ;
#9954=VECTOR ( 'NONE', #4848, 1000.000000000000000 ) ;
#9957=FACE_OUTER_BOUND ( 'NONE', #1050, .T. ) ;
#9983=LINE ( 'NONE', #2680, #14172 ) ;
#9984=DIRECTION ( 'NONE',  ( 0.000000000000000000, 5.551115123125748189E-17, 1.000000000000000000 ) ) ;
#10016=CARTESIAN_POINT ( 'NONE',  ( 0.000000000000000000, -2.914335439641035919E-13, -6.500000000000019540 ) ) ;
#10031=DIRECTION ( 'NONE',  ( 0.000000000000000000, 0.4999999999999999445, -0.8660254037844387076 ) ) ;
#10055=ORIENTED_EDGE ( 'NONE', *, *, #2250, .T. ) ;
#10059=VERTEX_POINT ( 'NONE', #14182 ) ;
#10080=DIRECTION ( 'NONE',  ( 0.000000000000000000, -5.551115123125748189E-17, -1.000000000000000000 ) ) ;
#10102=CARTESIAN_POINT ( 'NONE',  ( 0.05613245601034763665, 1.278525034529172544, 6.499999999999984013 ) ) ;
#10119=DIRECTION ( 'NONE',  ( 0.000000000000000000, 0.5000000000000008882, -0.8660254037844381525 ) ) ;
#10140=ORIENTED_EDGE ( 'NONE', *, *, #10411, .F. ) ;
#10141=DIRECTION ( 'NONE',  ( 0.000000000000000000, -5.551115123125747573E-17, -1.000000000000000000 ) ) ;
#10145=VECTOR ( 'NONE', #2108, 1000.000000000000000 ) ;
#10175=DIRECTION ( 'NONE',  ( 0.000000000000000000, -5.551115123125748189E-17, -1.000000000000000000 ) ) ;
#10189=ORIENTED_EDGE ( 'NONE', *, *, #11891, .T. ) ;
#10292=ORIENTED_EDGE ( 'NONE', *, *, #13245, .F. ) ;
#10300=EDGE_CURVE ( 'NONE', #9028, #7250, #11739, .T. ) ;
#10338=CARTESIAN_POINT ( 'NONE',  ( 0.000000000000000000, 0.000000000000000000, 0.000000000000000000 ) ) ;
#10340=VERTEX_POINT ( 'NONE', #5343 ) ;
#10341=LINE ( 'NONE', #7623, #3409 ) ;
#10378=CARTESIAN_POINT ( 'NONE',  ( 0.05533025579362366858, 4.993776679985823641, 4.350525068611912793 ) ) ;
#10411=EDGE_CURVE ( 'NONE', #12287, #6666, #6054, .T. ) ;
#10430=FACE_OUTER_BOUND ( 'NONE', #11953, .T. ) ;
#10431=AXIS2_PLACEMENT_3D ( 'NONE', #11393, #6893, #9891 ) ;
#10462=AXIS2_PLACEMENT_3D ( 'NONE', #11427, #4125, #16939 ) ;
#10474=DIRECTION ( 'NONE',  ( 0.000000000000000000, 0.5000000000000009992, 0.8660254037844381525 ) ) ;
#10488=CARTESIAN_POINT ( 'NONE',  ( 0.000000000000000000, 0.000000000000000000, 0.000000000000000000 ) ) ;
#10492=CARTESIAN_POINT ( 'NONE',  ( 7.512335209198389707E-14, -5.309483803148955516, -3.803704290982263814 ) ) ;
#10536=DIRECTION ( 'NONE',  ( 0.000000000000000000, 0.5000000000000009992, 0.8660254037844381525 ) ) ;
#10574=PRODUCT ( 'hex bolt gradeab fine_iso_ISO 8765 - M8x1.0 x 40 x 22-N', 'hex bolt gradeab fine_iso_ISO 8765 - M8x1.0 x 40 x 22-N', '', ( #6681 ) ) ;
#10581=STYLED_ITEM('',(#18566),#84);
#10657=LINE ( 'NONE', #1764, #612 ) ;
#10716=ORIENTED_EDGE ( 'NONE', *, *, #2, .F. ) ;
#10723=VERTEX_POINT ( 'NONE', #8138 ) ;
#10767=AXIS2_PLACEMENT_3D ( 'NONE', #3072, #8879, #3246 ) ;
#10777=DIRECTION ( 'NONE',  ( 0.000000000000000000, 5.551115123125747573E-17, 1.000000000000000000 ) ) ;
#10778=CARTESIAN_POINT ( 'NONE',  ( 5.299999999999998934, -7.505553499465293932, 1.040834085586084257E-14 ) ) ;
#10903=EDGE_CURVE ( 'NONE', #9885, #16487, #9367, .T. ) ;
#10936=CARTESIAN_POINT ( 'NONE',  ( 5.299999999999998934, 3.752776749732435135, 6.499999999999981348 ) ) ;
#10979=ADVANCED_FACE ( 'NONE', ( #14199 ), #8391, .F. ) ;
#10984=EDGE_CURVE ( 'NONE', #6666, #1661, #3988, .T. ) ;
#10999=EDGE_CURVE ( 'NONE', #9582, #850, #12375, .T. ) ;
#11014=LINE ( 'NONE', #14009, #11623 ) ;
#11018=DIRECTION ( 'NONE',  ( 0.000000000000000000, -5.551115123125748806E-17, -1.000000000000000000 ) ) ;
#11023=VERTEX_POINT ( 'NONE', #16034 ) ;
#11031=CARTESIAN_POINT ( 'NONE',  ( 0.06682554136346589846, -6.264794173742427752, -2.149058192116912291 ) ) ;
#11034=CARTESIAN_POINT ( 'NONE',  ( 5.299999999999998934, 3.752776749732559924, -6.500000000000061284 ) ) ;
#11089=TOROIDAL_SURFACE ( 'NONE', #8393, 4.400000000000000355, 0.4000000000000000222 ) ;
#11090=ORIENTED_EDGE ( 'NONE', *, *, #12702, .F. ) ;
#11099=EDGE_LOOP ( 'NONE', ( #5074, #6517, #15389, #14480, #3619, #12000 ) ) ;
#11133=CARTESIAN_POINT ( 'NONE',  ( 0.2578475836321609260, -6.890627091270527416, -1.065083781909184513 ) ) ;
#11205=PRODUCT_DEFINITION_SHAPE ( 'NONE', 'NONE',  #3491 ) ;
#11229=CARTESIAN_POINT ( 'NONE',  ( 0.000000000000000000, 2.678141147339130316E-16, -4.000000000000024869 ) ) ;
#11242=EDGE_CURVE ( 'NONE', #1357, #1661, #4869, .T. ) ;
#11243=EDGE_CURVE ( 'NONE', #1357, #12287, #17720, .T. ) ;
#11290=ADVANCED_FACE ( 'NONE', ( #18148 ), #8231, .T. ) ;
#11294=EDGE_CURVE ( 'NONE', #18326, #9028, #7013, .T. ) ;
#11327=DIRECTION ( 'NONE',  ( 0.000000000000000000, 1.000000000000000000, 2.775557561562874095E-16 ) ) ;
#11393=CARTESIAN_POINT ( 'NONE',  ( 5.299999999999998934, -3.752776749732712691, -6.500000000000033751 ) ) ;
#11417=ORIENTED_EDGE ( 'NONE', *, *, #17269, .F. ) ;
#11427=CARTESIAN_POINT ( 'NONE',  ( 4.699999999999995737, 6.499999999999901412, 2.428612866367529932E-14 ) ) ;
#11480=DIRECTION ( 'NONE',  ( 0.000000000000000000, -0.5000000000000008882, 0.8660254037844381525 ) ) ;
#11579=DIRECTION ( 'NONE',  ( 0.000000000000000000, -5.551115123125747573E-17, -1.000000000000000000 ) ) ;
#11589=( NAMED_UNIT ( * ) SI_UNIT ( $, .STERADIAN. ) SOLID_ANGLE_UNIT ( ) );
#11623=VECTOR ( 'NONE', #16798, 1000.000000000000000 ) ;
#11643=EDGE_LOOP ( 'NONE', ( #14449, #6344, #17158, #9752, #3471, #388 ) ) ;
#11648=CONICAL_SURFACE ( 'NONE', #3884, 3.445500000000021767, 0.7853981633974420618 ) ;
#11659=EDGE_CURVE ( 'NONE', #8947, #15932, #1195, .T. ) ;
#11677=VECTOR ( 'NONE', #14849, 1000.000000000000000 ) ;
#11682=CONICAL_SURFACE ( 'NONE', #4503, 6.500000000000039968, 1.047197551196600296 ) ;
#11705=DIRECTION ( 'NONE',  ( 0.000000000000000000, 1.000000000000000000, -3.330669073875448914E-16 ) ) ;
#11719=PLANE ( 'NONE',  #720 ) ;
#11726=CARTESIAN_POINT ( 'NONE',  ( 7.705628127761821045E-14, -5.948846446049038228, 2.696295709017791253 ) ) ;
#11739=B_SPLINE_CURVE_WITH_KNOTS ( 'NONE', 3,
 ( #8058, #6468, #6370, #17879, #12286, #16194 ),
 .UNSPECIFIED., .F., .F.,
 ( 4, 2, 4 ),
 ( 0.02294124189247833887, 0.02484059228081024473, 0.02673994266914214712 ),
 .UNSPECIFIED. ) ;
#11746=CARTESIAN_POINT ( 'NONE',  ( 0.5805565836007609004, -3.752776749732685158, 6.500000000000043521 ) ) ;
#11752=PLANE ( 'NONE',  #6311 ) ;
#11786=VECTOR ( 'NONE', #3814, 1000.000000000000000 ) ;
#11802=EDGE_CURVE ( 'NONE', #17620, #9582, #1761, .T. ) ;
#11804=CARTESIAN_POINT ( 'NONE',  ( 0.000000000000000000, 0.000000000000000000, 0.000000000000000000 ) ) ;
#11860=CARTESIAN_POINT ( 'NONE',  ( 4.699999999999995737, 0.000000000000000000, 0.000000000000000000 ) ) ;
#11887=CARTESIAN_POINT ( 'NONE',  ( 0.000000000000000000, 0.000000000000000000, 0.000000000000000000 ) ) ;
#11890=ORIENTED_EDGE ( 'NONE', *, *, #1415, .T. ) ;
#11891=EDGE_CURVE ( 'NONE', #4210, #10723, #8765, .T. ) ;
#11921=CARTESIAN_POINT ( 'NONE',  ( -6.390016554086442547E-15, -0.6346842323188388590, 6.499999999999983125 ) ) ;
#11945=LINE ( 'NONE', #12226, #14367 ) ;
#11953=EDGE_LOOP ( 'NONE', ( #1429, #3731, #7781, #7417, #9790, #8534 ) ) ;
#11963=CARTESIAN_POINT ( 'NONE',  ( 5.299999999999998934, -3.752776749732685158, 6.500000000000043521 ) ) ;
#11971=ORIENTED_EDGE ( 'NONE', *, *, #15921, .T. ) ;
#11980=EDGE_CURVE ( 'NONE', #9028, #12345, #2222, .T. ) ;
#12000=ORIENTED_EDGE ( 'NONE', *, *, #7126, .F. ) ;
#12043=DIRECTION ( 'NONE',  ( 0.000000000000000000, -5.551115123125747573E-17, -1.000000000000000000 ) ) ;
#12059=AXIS2_PLACEMENT_3D ( 'NONE', #17204, #17109, #10175 ) ;
#12072=AXIS2_PLACEMENT_3D ( 'NONE', #1143, #15362, #8340 ) ;
#12098=CARTESIAN_POINT ( 'NONE',  ( 0.4033376246893092820, -4.059728990630953938, -5.968343123267158212 ) ) ;
#12102=TOROIDAL_SURFACE ( 'NONE', #13896, 4.400000000000000355, 0.4000000000000000222 ) ;
#12113=AXIS2_PLACEMENT_3D ( 'NONE', #15979, #1323, #7291 ) ;
#12164=DIRECTION ( 'NONE',  ( 0.000000000000000000, -5.551115123125746341E-17, -1.000000000000000000 ) ) ;
#12175=ADVANCED_BREP_SHAPE_REPRESENTATION ( '', ( #84, #16217 ), #15033 ) ;
#12178=CARTESIAN_POINT ( 'NONE',  ( 4.699999999999995737, 0.000000000000000000, 0.000000000000000000 ) ) ;
#12183=CARTESIAN_POINT ( 'NONE',  ( 1.614557735192997546E-14, 5.469921996229766492, -3.525817189091522863 ) ) ;
#12205=DIRECTION ( 'NONE',  ( 1.000000000000000000, 0.000000000000000000, 0.000000000000000000 ) ) ;
#12218=CARTESIAN_POINT ( 'NONE',  ( 5.699999999999996625, 2.678141147339113553E-16, -4.000000000000000000 ) ) ;
#12224=ADVANCED_FACE ( 'NONE', ( #3462 ), #12102, .F. ) ;
#12226=CARTESIAN_POINT ( 'NONE',  ( 5.299999999999998934, -3.752776749732712691, -6.500000000000033751 ) ) ;
#12286=CARTESIAN_POINT ( 'NONE',  ( 0.4042117618285392400, -3.141900367810186889, -6.500000000000063061 ) ) ;
#12287=VERTEX_POINT ( 'NONE', #4852 ) ;
#12333=CARTESIAN_POINT ( 'NONE',  ( 4.699999999999995737, 3.752776749732435135, 6.499999999999981348 ) ) ;
#12337=ORIENTED_EDGE ( 'NONE', *, *, #18348, .F. ) ;
#12345=VERTEX_POINT ( 'NONE', #4955 ) ;
#12375=CIRCLE ( 'NONE', #13257, 6.500000000000039968 ) ;
#12376=VECTOR ( 'NONE', #10536, 999.9999999999998863 ) ;
#12392=CARTESIAN_POINT ( 'NONE',  ( 45.30000000000000426, 0.000000000000000000, 0.000000000000000000 ) ) ;
#12409=DIRECTION ( 'NONE',  ( 0.000000000000000000, -5.551115123125747573E-17, -1.000000000000000000 ) ) ;
#12436=DIRECTION ( 'NONE',  ( 0.000000000000000000, -1.000000000000000000, 3.330669073875448914E-16 ) ) ;
#12465=ORIENTED_EDGE ( 'NONE', *, *, #6742, .F. ) ;
#12483=CARTESIAN_POINT ( 'NONE',  ( 5.699999999999996625, 7.830936570423733112E-16, 4.400000000000027889 ) ) ;
#12486=ADVANCED_FACE ( 'NONE', ( #8133 ), #13847, .T. ) ;
#12493=ADVANCED_FACE ( 'NONE', ( #8790 ), #4469, .T. ) ;
#12535=ORIENTED_EDGE ( 'NONE', *, *, #1823, .T. ) ;
#12549=ORIENTED_EDGE ( 'NONE', *, *, #12702, .T. ) ;
#12550=ADVANCED_FACE ( 'NONE', ( #7115 ), #9922, .F. ) ;
#12557=CARTESIAN_POINT ( 'NONE',  ( 4.699999999999995737, -3.752776749732685158, 6.500000000000043521 ) ) ;
#12577=AXIS2_PLACEMENT_3D ( 'NONE', #9829, #1134, #1332 ) ;
#12649=CARTESIAN_POINT ( 'NONE',  ( 0.4037800551813724992, 7.199367570657603466, 0.5303295852573092217 ) ) ;
#12654=CARTESIAN_POINT ( 'NONE',  ( 5.299999999999998934, 3.752776749732559924, -6.500000000000061284 ) ) ;
#12684=AXIS2_PLACEMENT_3D ( 'NONE', #13711, #16322, #17634 ) ;
#12702=EDGE_CURVE ( 'NONE', #1661, #6666, #764, .T. ) ;
#12718=DIRECTION ( 'NONE',  ( 0.000000000000000000, 5.551115123125748189E-17, 1.000000000000000000 ) ) ;
#12752=DIRECTION ( 'NONE',  ( 0.000000000000000000, -5.551115123125747573E-17, -1.000000000000000000 ) ) ;
#12758=EDGE_LOOP ( 'NONE', ( #10140, #16214, #2757, #4821 ) ) ;
#12760=EDGE_LOOP ( 'NONE', ( #14507, #4218, #8017, #9636, #10292, #18290 ) ) ;
#12819=ORIENTED_EDGE ( 'NONE', *, *, #15441, .T. ) ;
#12833=ORIENTED_EDGE ( 'NONE', *, *, #16753, .T. ) ;
#12842=CARTESIAN_POINT ( 'NONE',  ( 7.349987227641307482E-14, -5.469921996229923700, 3.525817189091461579 ) ) ;
#12853=CARTESIAN_POINT ( 'NONE',  ( 4.699999999999995737, 3.752776749732559924, -6.500000000000061284 ) ) ;
#12864=DIRECTION ( 'NONE',  ( 0.000000000000000000, 5.551115123125748189E-17, 1.000000000000000000 ) ) ;
#12884=AXIS2_PLACEMENT_3D ( 'NONE', #12654, #269, #1857 ) ;
#12887=CIRCLE ( 'NONE', #10767, 6.500000000000039968 ) ;
#12935=CARTESIAN_POINT ( 'NONE',  ( 4.699999999999995737, -3.752776749732712691, -6.500000000000033751 ) ) ;
#12947=AXIS2_PLACEMENT_3D ( 'NONE', #12178, #13584, #17868 ) ;
#13025=AXIS2_PLACEMENT_3D ( 'NONE', #3170, #8881, #451 ) ;
#13026=AXIS2_PLACEMENT_3D ( 'NONE', #14832, #7823, #12043 ) ;
#13111=CARTESIAN_POINT ( 'NONE',  ( 5.299999999999998934, 3.752776749732435135, 6.499999999999981348 ) ) ;
#13149=EDGE_CURVE ( 'NONE', #15640, #7354, #15766, .T. ) ;
#13245=EDGE_CURVE ( 'NONE', #7590, #14582, #5016, .T. ) ;
#13257=AXIS2_PLACEMENT_3D ( 'NONE', #1103, #6796, #8294 ) ;
#13296=CYLINDRICAL_SURFACE ( 'NONE', #17912, 4.000000000000024869 ) ;
#13330=( LENGTH_UNIT ( ) NAMED_UNIT ( * ) SI_UNIT ( .MILLI., .METRE. ) );
#13390=ORIENTED_EDGE ( 'NONE', *, *, #820, .T. ) ;
#13427=DIRECTION ( 'NONE',  ( 0.000000000000000000, 5.551115123125748189E-17, 1.000000000000000000 ) ) ;
#13456=LINE ( 'NONE', #14933, #11677 ) ;
#13553=AXIS2_PLACEMENT_3D ( 'NONE', #15410, #4090, #9984 ) ;
#13584=DIRECTION ( 'NONE',  ( -1.000000000000000000, 0.000000000000000000, 0.000000000000000000 ) ) ;
#13599=CONICAL_SURFACE ( 'NONE', #1365, 6.500000000000039968, 1.047197551196600296 ) ;
#13600=CARTESIAN_POINT ( 'NONE',  ( 5.299999999999998934, 3.608224830031735584E-16, 6.499999999999999112 ) ) ;
#13645=ADVANCED_FACE ( 'NONE', ( #7991 ), #4995, .T. ) ;
#13678=CARTESIAN_POINT ( 'NONE',  ( 0.4033376246892572681, 7.198601258566914574, -0.5316568767329080680 ) ) ;
#13693=CARTESIAN_POINT ( 'NONE',  ( 4.699999999999995737, 3.752776749732435135, 6.499999999999981348 ) ) ;
#13711=CARTESIAN_POINT ( 'NONE',  ( 5.699999999999996625, 0.000000000000000000, 0.000000000000000000 ) ) ;
#13722=LINE ( 'NONE', #12333, #6426 ) ;
#13728=ADVANCED_FACE ( 'NONE', ( #15488, #1614 ), #3792, .T. ) ;
#13734=ORIENTED_EDGE ( 'NONE', *, *, #8924, .T. ) ;
#13774=CYLINDRICAL_SURFACE ( 'NONE', #6929, 6.500000000000039968 ) ;
#13805=CARTESIAN_POINT ( 'NONE',  ( 4.699999999999995737, 3.752776749732435135, 6.499999999999981348 ) ) ;
#13806=CIRCLE ( 'NONE', #5738, 6.500000000000039968 ) ;
#13847=PLANE ( 'NONE',  #4622 ) ;
#13851=AXIS2_PLACEMENT_3D ( 'NONE', #14102, #2876, #16985 ) ;
#13866=VECTOR ( 'NONE', #8578, 999.9999999999998863 ) ;
#13896=AXIS2_PLACEMENT_3D ( 'NONE', #1874, #17855, #8988 ) ;
#13908=DIRECTION ( 'NONE',  ( 0.000000000000000000, -5.551115123125748189E-17, -1.000000000000000000 ) ) ;
#13944=CARTESIAN_POINT ( 'NONE',  ( 4.699999999999995737, 6.499999999999901412, 2.428612866367529932E-14 ) ) ;
#14009=CARTESIAN_POINT ( 'NONE',  ( 0.000000000000000000, 4.351979364426085531E-16, -6.500000000000039968 ) ) ;
#14016=CONICAL_SURFACE ( 'NONE', #5642, 6.500000000000039968, 1.047197551196600296 ) ;
#14019=ORIENTED_EDGE ( 'NONE', *, *, #2755, .F. ) ;
#14057=CARTESIAN_POINT ( 'NONE',  ( 0.4037800551814025307, 4.058962678540093627, -5.969670414742754616 ) ) ;
#14102=CARTESIAN_POINT ( 'NONE',  ( 5.299999999999998934, 0.000000000000000000, 0.000000000000000000 ) ) ;
#14125=CARTESIAN_POINT ( 'NONE',  ( 0.4037800551814653138, -7.199367570657762450, -0.5303295852573244318 ) ) ;
#14134=CARTESIAN_POINT ( 'NONE',  ( 0.000000000000000000, -4.857225732735059864E-14, 6.500000000000037303 ) ) ;
#14164=ADVANCED_FACE ( 'NONE', ( #15636 ), #14321, .T. ) ;
#14165=PRODUCT_DEFINITION_FORMATION_WITH_SPECIFIED_SOURCE ( 'ANY', '', #10574, .NOT_KNOWN. ) ;
#14172=VECTOR ( 'NONE', #8388, 1000.000000000000000 ) ;
#14182=CARTESIAN_POINT ( 'NONE',  ( 44.74549999999999272, 2.678141147339113553E-16, -4.000000000000000000 ) ) ;
#14190=ADVANCED_FACE ( 'NONE', ( #8328 ), #8431, .T. ) ;
#14199=FACE_OUTER_BOUND ( 'NONE', #6031, .T. ) ;
#14224=ORIENTED_EDGE ( 'NONE', *, *, #17491, .T. ) ;
#14252=ORIENTED_EDGE ( 'NONE', *, *, #2628, .T. ) ;
#14269=CARTESIAN_POINT ( 'NONE',  ( 0.000000000000000000, -2.914335439641035919E-13, -6.500000000000019540 ) ) ;
#14285=ORIENTED_EDGE ( 'NONE', *, *, #11980, .T. ) ;
#14307=DIRECTION ( 'NONE',  ( 0.000000000000000000, -5.551115123125747573E-17, -1.000000000000000000 ) ) ;
#14321=PLANE ( 'NONE',  #10462 ) ;
#14367=VECTOR ( 'NONE', #6422, 1000.000000000000000 ) ;
#14376=CARTESIAN_POINT ( 'NONE',  ( 5.299999999999998934, 0.000000000000000000, 0.000000000000000000 ) ) ;
#14395=DIRECTION ( 'NONE',  ( -1.000000000000000000, 0.000000000000000000, 0.000000000000000000 ) ) ;
#14400=CARTESIAN_POINT ( 'NONE',  ( 0.000000000000000000, 0.000000000000000000, 0.000000000000000000 ) ) ;
#14414=CIRCLE ( 'NONE', #1279, 6.500000000000039968 ) ;
#14449=ORIENTED_EDGE ( 'NONE', *, *, #9799, .F. ) ;
#14453=ORIENTED_EDGE ( 'NONE', *, *, #1506, .F. ) ;
#14463=EDGE_LOOP ( 'NONE', ( #17636, #391, #10189, #8632, #14453, #4416 ) ) ;
#14480=ORIENTED_EDGE ( 'NONE', *, *, #9063, .F. ) ;
#14494=CARTESIAN_POINT ( 'NONE',  ( 0.000000000000000000, 0.000000000000000000, 0.000000000000000000 ) ) ;
#14496=DIRECTION ( 'NONE',  ( 1.000000000000000000, 0.000000000000000000, 0.000000000000000000 ) ) ;
#14507=ORIENTED_EDGE ( 'NONE', *, *, #13149, .F. ) ;
#14512=DIRECTION ( 'NONE',  ( 0.000000000000000000, 5.551115123125748189E-17, 1.000000000000000000 ) ) ;
#14563=ORIENTED_EDGE ( 'NONE', *, *, #871, .F. ) ;
#14573=CARTESIAN_POINT ( 'NONE',  ( 5.299999999999996270, -2.442490654175344586E-16, -4.400000000000027889 ) ) ;
#14582=VERTEX_POINT ( 'NONE', #4453 ) ;
#14586=EDGE_LOOP ( 'NONE', ( #16468, #12535, #5312 ) ) ;
#14587=CARTESIAN_POINT ( 'NONE',  ( 0.000000000000000000, 5.629165124598801917, 3.250000000000037748 ) ) ;
#14608=CARTESIAN_POINT ( 'NONE',  ( 45.30000000000000426, 0.000000000000000000, 0.000000000000000000 ) ) ;
#14689=VECTOR ( 'NONE', #11327, 1000.000000000000000 ) ;
#14747=CARTESIAN_POINT ( 'NONE',  ( 4.699999999999995737, 3.752776749732559924, -6.500000000000061284 ) ) ;
#14767=ORIENTED_EDGE ( 'NONE', *, *, #10999, .T. ) ;
#14808=EDGE_CURVE ( 'NONE', #10723, #646, #16318, .T. ) ;
#14823=CARTESIAN_POINT ( 'NONE',  ( 0.000000000000000000, 0.000000000000000000, 0.000000000000000000 ) ) ;
#14832=CARTESIAN_POINT ( 'NONE',  ( 0.000000000000000000, 0.000000000000000000, 0.000000000000000000 ) ) ;
#14849=DIRECTION ( 'NONE',  ( -1.000000000000000000, 0.000000000000000000, 0.000000000000000000 ) ) ;
#14933=CARTESIAN_POINT ( 'NONE',  ( 5.299999999999998934, 7.505553499465141165, -1.387778780781445676E-14 ) ) ;
#15033=( GEOMETRIC_REPRESENTATION_CONTEXT ( 3 ) GLOBAL_UNCERTAINTY_ASSIGNED_CONTEXT ( ( #15452 ) ) GLOBAL_UNIT_ASSIGNED_CONTEXT ( ( #4462, #3067, #11589 ) ) REPRESENTATION_CONTEXT ( 'NONE', 'WORKASPACE' ) );
#15159=CARTESIAN_POINT ( 'NONE',  ( 0.06682554136340505824, 4.993536075455400791, -4.350941807883202728 ) ) ;
#15251=ORIENTED_EDGE ( 'NONE', *, *, #18348, .T. ) ;
#15268=FACE_OUTER_BOUND ( 'NONE', #948, .T. ) ;
#15276=AXIS2_PLACEMENT_3D ( 'NONE', #5811, #4059, #10119 ) ;
#15295=CIRCLE ( 'NONE', #17980, 6.500000000000039968 ) ;
#15332=DIRECTION ( 'NONE',  ( 1.000000000000000000, 0.000000000000000000, 0.000000000000000000 ) ) ;
#15352=EDGE_LOOP ( 'NONE', ( #12833, #7377, #10055 ) ) ;
#15362=DIRECTION ( 'NONE',  ( -1.000000000000000000, 0.000000000000000000, 0.000000000000000000 ) ) ;
#15372=DIRECTION ( 'NONE',  ( 0.000000000000000000, 1.000000000000000000, -1.779758311459928026E-16 ) ) ;
#15380=ORIENTED_EDGE ( 'NONE', *, *, #1506, .T. ) ;
#15389=ORIENTED_EDGE ( 'NONE', *, *, #9149, .F. ) ;
#15410=CARTESIAN_POINT ( 'NONE',  ( 45.30000000000000426, 0.000000000000000000, 0.000000000000000000 ) ) ;
#15436=CARTESIAN_POINT ( 'NONE',  ( 0.4053525175236978306, 3.145852061456188675, -6.500000000000061284 ) ) ;
#15441=EDGE_CURVE ( 'NONE', #15932, #11023, #5807, .T. ) ;
#15450=ADVANCED_FACE ( 'NONE', ( #9939 ), #13296, .T. ) ;
#15452=UNCERTAINTY_MEASURE_WITH_UNIT (LENGTH_MEASURE( 1.000000000000000082E-05 ), #4462, 'distance_accuracy_value', 'NONE');
#15458=CARTESIAN_POINT ( 'NONE',  ( 4.699999999999995737, -3.752776749732712691, -6.500000000000033751 ) ) ;
#15488=FACE_BOUND ( 'NONE', #4796, .T. ) ;
#15522=CARTESIAN_POINT ( 'NONE',  ( 0.5805565836007609004, 7.505553499465141165, -1.387778780781445676E-14 ) ) ;
#15523=CARTESIAN_POINT ( 'NONE',  ( 5.299999999999998934, -7.505553499465293932, 1.040834085586084257E-14 ) ) ;
#15532=VECTOR ( 'NONE', #3942, 999.9999999999998863 ) ;
#15588=ORIENTED_EDGE ( 'NONE', *, *, #11802, .F. ) ;
#15597=DIRECTION ( 'NONE',  ( 0.000000000000000000, 5.551115123125747573E-17, 1.000000000000000000 ) ) ;
#15602=DIRECTION ( 'NONE',  ( 0.000000000000000000, -0.5000000000000017764, -0.8660254037844377084 ) ) ;
#15636=FACE_OUTER_BOUND ( 'NONE', #16835, .T. ) ;
#15640=VERTEX_POINT ( 'NONE', #9175 ) ;
#15680=FACE_OUTER_BOUND ( 'NONE', #15352, .T. ) ;
#15728=CARTESIAN_POINT ( 'NONE',  ( 45.30000000000000426, 1.912636715672988680E-16, 3.445500000000021767 ) ) ;
#15754=ORIENTED_EDGE ( 'NONE', *, *, #871, .T. ) ;
#15764=EDGE_CURVE ( 'NONE', #7124, #9028, #17866, .T. ) ;
#15766=LINE ( 'NONE', #2950, #1630 ) ;
#15776=ORIENTED_EDGE ( 'NONE', *, *, #3554, .T. ) ;
#15799=CARTESIAN_POINT ( 'NONE',  ( 44.74549999999999272, 0.000000000000000000, 0.000000000000000000 ) ) ;
#15835=DIRECTION ( 'NONE',  ( 1.000000000000000000, 0.000000000000000000, 0.000000000000000000 ) ) ;
#15837=VERTEX_POINT ( 'NONE', #5785 ) ;
#15884=DIRECTION ( 'NONE',  ( 0.000000000000000000, 0.5000000000000017764, 0.8660254037844375974 ) ) ;
#15888=EDGE_CURVE ( 'NONE', #9582, #7975, #12887, .T. ) ;
#15898=AXIS2_PLACEMENT_3D ( 'NONE', #17834, #7734, #3613 ) ;
#15905=CARTESIAN_POINT ( 'NONE',  ( 0.5805565836007609004, -3.752776749732685158, 6.500000000000043521 ) ) ;
#15915=AXIS2_PLACEMENT_3D ( 'NONE', #884, #6691, #8188 ) ;
#15921=EDGE_CURVE ( 'NONE', #5963, #10059, #7205, .T. ) ;
#15927=AXIS2_PLACEMENT_3D ( 'NONE', #12483, #15372, #17042 ) ;
#15932=VERTEX_POINT ( 'NONE', #8788 ) ;
#15945=CLOSED_SHELL ( 'NONE', ( #12224, #12493, #7896, #13645, #13728, #15450, #4273, #10979, #3076, #14190, #12486, #11290, #14164, #7331, #6884, #16509, #5710, #5166, #1159, #4056, #7125, #8104, #4912, #3556, #12550, #9261, #6997, #18417, #16202 ) ) ;
#15979=CARTESIAN_POINT ( 'NONE',  ( 4.699999999999995737, 0.000000000000000000, 0.000000000000000000 ) ) ;
#15994=CARTESIAN_POINT ( 'NONE',  ( 0.5805565836007609004, 3.752776749732435135, 6.499999999999981348 ) ) ;
#15999=EDGE_CURVE ( 'NONE', #16487, #4375, #9232, .T. ) ;
#16010=FACE_OUTER_BOUND ( 'NONE', #2877, .T. ) ;
#16017=DIRECTION ( 'NONE',  ( -1.000000000000000000, 0.000000000000000000, 0.000000000000000000 ) ) ;
#16022=CARTESIAN_POINT ( 'NONE',  ( 5.299999999999996270, 7.830936570423732126E-16, 4.400000000000027889 ) ) ;
#16033=DIRECTION ( 'NONE',  ( 0.000000000000000000, -0.5000000000000008882, 0.8660254037844381525 ) ) ;
#16034=CARTESIAN_POINT ( 'NONE',  ( 4.699999999999995737, -5.629165124598996428, -3.250000000000020428 ) ) ;
#16047=ORIENTED_EDGE ( 'NONE', *, *, #3219, .T. ) ;
#16055=EDGE_LOOP ( 'NONE', ( #15754, #5663, #3391 ) ) ;
#16092=EDGE_CURVE ( 'NONE', #3553, #7250, #11945, .T. ) ;
#16095=CARTESIAN_POINT ( 'NONE',  ( 0.000000000000000000, -5.629165124598996428, -3.250000000000020428 ) ) ;
#16134=AXIS2_PLACEMENT_3D ( 'NONE', #15799, #14395, #5874 ) ;
#16194=CARTESIAN_POINT ( 'NONE',  ( 0.5805565836007609004, -3.752776749732712691, -6.500000000000033751 ) ) ;
#16202=ADVANCED_FACE ( 'NONE', ( #5302 ), #11089, .F. ) ;
#16211=CARTESIAN_POINT ( 'NONE',  ( 45.30000000000000426, 0.000000000000000000, 0.000000000000000000 ) ) ;
#16214=ORIENTED_EDGE ( 'NONE', *, *, #11243, .F. ) ;
#16217=AXIS2_PLACEMENT_3D ( 'NONE', #5781, #6037, #8961 ) ;
#16281=DIRECTION ( 'NONE',  ( 0.000000000000000000, -5.551115123125747573E-17, -1.000000000000000000 ) ) ;
#16318=LINE ( 'NONE', #13805, #10145 ) ;
#16322=DIRECTION ( 'NONE',  ( 1.000000000000000000, 0.000000000000000000, 0.000000000000000000 ) ) ;
#16392=DIRECTION ( 'NONE',  ( -1.000000000000000000, 0.000000000000000000, 0.000000000000000000 ) ) ;
#16468=ORIENTED_EDGE ( 'NONE', *, *, #128, .T. ) ;
#16487=VERTEX_POINT ( 'NONE', #7905 ) ;
#16495=ORIENTED_EDGE ( 'NONE', *, *, #9742, .T. ) ;
#16509=ADVANCED_FACE ( 'NONE', ( #10430 ), #796, .F. ) ;
#16575=AXIS2_PLACEMENT_3D ( 'NONE', #14494, #9823, #1580 ) ;
#16644=EDGE_LOOP ( 'NONE', ( #14019, #15251, #17027, #190, #17536, #2473 ) ) ;
#16719=DIRECTION ( 'NONE',  ( 0.000000000000000000, -0.8660254037844381525, 0.5000000000000008882 ) ) ;
#16721=CARTESIAN_POINT ( 'NONE',  ( 0.05613245601037662041, 1.278525034529053306, -6.500000000000062172 ) ) ;
#16753=EDGE_CURVE ( 'NONE', #9192, #850, #6941, .T. ) ;
#16795=CONICAL_SURFACE ( 'NONE', #1860, 3.445500000000021767, 0.7853981633974420618 ) ;
#16798=DIRECTION ( 'NONE',  ( -1.000000000000000000, 0.000000000000000000, 0.000000000000000000 ) ) ;
#16813=DIRECTION ( 'NONE',  ( 0.000000000000000000, -5.551115123125747573E-17, -1.000000000000000000 ) ) ;
#16835=EDGE_LOOP ( 'NONE', ( #1741, #12819, #15380 ) ) ;
#16846=ORIENTED_EDGE ( 'NONE', *, *, #15764, .T. ) ;
#16847=LINE ( 'NONE', #7200, #14689 ) ;
#16877=AXIS2_PLACEMENT_3D ( 'NONE', #3827, #5232, #18347 ) ;
#16889=EDGE_CURVE ( 'NONE', #15932, #9192, #17693, .T. ) ;
#16937=ORIENTED_EDGE ( 'NONE', *, *, #9063, .T. ) ;
#16939=DIRECTION ( 'NONE',  ( 0.000000000000000000, -5.551115123125748189E-17, -1.000000000000000000 ) ) ;
#16985=DIRECTION ( 'NONE',  ( 0.000000000000000000, -5.551115123125748189E-17, -1.000000000000000000 ) ) ;
#16991=CARTESIAN_POINT ( 'NONE',  ( 4.699999999999995737, -7.505553499465293932, 1.040834085586084257E-14 ) ) ;
#16994=CARTESIAN_POINT ( 'NONE',  ( 5.699999999999996625, 0.000000000000000000, 0.000000000000000000 ) ) ;
#17007=CARTESIAN_POINT ( 'NONE',  ( 0.5805565836007747782, -7.505553499465293932, 1.040834085586084257E-14 ) ) ;
#17018=ORIENTED_EDGE ( 'NONE', *, *, #10300, .T. ) ;
#17027=ORIENTED_EDGE ( 'NONE', *, *, #18094, .F. ) ;
#17032=EDGE_CURVE ( 'NONE', #5963, #12287, #8055, .T. ) ;
#17042=DIRECTION ( 'NONE',  ( 0.000000000000000000, 1.779758311459927780E-16, 1.000000000000000000 ) ) ;
#17074=VERTEX_POINT ( 'NONE', #1493 ) ;
#17109=DIRECTION ( 'NONE',  ( 1.000000000000000000, 0.000000000000000000, 0.000000000000000000 ) ) ;
#17158=ORIENTED_EDGE ( 'NONE', *, *, #10300, .F. ) ;
#17202=APPLICATION_CONTEXT ( 'automotive_design' ) ;
#17204=CARTESIAN_POINT ( 'NONE',  ( 4.699999999999995737, 6.499999999999901412, 2.428612866367529932E-14 ) ) ;
#17233=B_SPLINE_CURVE_WITH_KNOTS ( 'NONE', 3,
 ( #9374, #13678, #17972, #9103, #17791, #7875 ),
 .UNSPECIFIED., .F., .F.,
 ( 4, 2, 4 ),
 ( 2.380733002060942798E-07, 0.001898835937927345141, 0.003797433802554483605 ),
 .UNSPECIFIED. ) ;
#17252=CARTESIAN_POINT ( 'NONE',  ( 4.699999999999995737, -7.505553499465293932, 1.040834085586084257E-14 ) ) ;
#17269=EDGE_CURVE ( 'NONE', #7354, #9885, #5444, .T. ) ;
#17282=ORIENTED_EDGE ( 'NONE', *, *, #13245, .T. ) ;
#17299=CARTESIAN_POINT ( 'NONE',  ( 0.4033376246892568795, 4.059728990630770085, 5.968343123267169759 ) ) ;
#17300=CARTESIAN_POINT ( 'NONE',  ( 0.4037800551814316186, -4.058962678540228630, 5.969670414742723530 ) ) ;
#17364=VERTEX_POINT ( 'NONE', #5585 ) ;
#17369=AXIS2_PLACEMENT_3D ( 'NONE', #13111, #17489, #11705 ) ;
#17372=CARTESIAN_POINT ( 'NONE',  ( 0.5805565836007609004, 3.752776749732435135, 6.499999999999981348 ) ) ;
#17406=CONICAL_SURFACE ( 'NONE', #1584, 6.500000000000039968, 1.047197551196600296 ) ;
#17412=CARTESIAN_POINT ( 'NONE',  ( 4.699999999999995737, 6.499999999999901412, 2.428612866367529932E-14 ) ) ;
#17489=DIRECTION ( 'NONE',  ( 0.000000000000000000, -3.330669073875448914E-16, -1.000000000000000000 ) ) ;
#17491=EDGE_CURVE ( 'NONE', #4210, #17364, #14414, .T. ) ;
#17508=FACE_OUTER_BOUND ( 'NONE', #3415, .T. ) ;
#17536=ORIENTED_EDGE ( 'NONE', *, *, #16889, .F. ) ;
#17620=VERTEX_POINT ( 'NONE', #2285 ) ;
#17634=DIRECTION ( 'NONE',  ( 0.000000000000000000, -5.551115123125748189E-17, -1.000000000000000000 ) ) ;
#17636=ORIENTED_EDGE ( 'NONE', *, *, #3554, .F. ) ;
#17681=EDGE_CURVE ( 'NONE', #10723, #7354, #5753, .T. ) ;
#17693=LINE ( 'NONE', #10778, #3041 ) ;
#17720=CIRCLE ( 'NONE', #18353, 4.000000000000024869 ) ;
#17739=LINE ( 'NONE', #893, #12376 ) ;
#17786=DIRECTION ( 'NONE',  ( 0.000000000000000000, -5.551115123125747573E-17, -1.000000000000000000 ) ) ;
#17791=CARTESIAN_POINT ( 'NONE',  ( 6.212139635163038687E-15, 5.948846446048876579, -2.696295709017856534 ) ) ;
#17834=CARTESIAN_POINT ( 'NONE',  ( 4.699999999999995737, 0.000000000000000000, 0.000000000000000000 ) ) ;
#17855=DIRECTION ( 'NONE',  ( 1.000000000000000000, 0.000000000000000000, 0.000000000000000000 ) ) ;
#17866=B_SPLINE_CURVE_WITH_KNOTS ( 'NONE', 3,
 ( #9821, #15436, #1217, #16721, #1126, #10016 ),
 .UNSPECIFIED., .F., .F.,
 ( 4, 2, 4 ),
 ( 0.01913986446880888009, 0.02104055318064360774, 0.02294124189247833887 ),
 .UNSPECIFIED. ) ;
#17868=DIRECTION ( 'NONE',  ( 0.000000000000000000, 5.551115123125747573E-17, 1.000000000000000000 ) ) ;
#17873=CARTESIAN_POINT ( 'NONE',  ( 0.01372220897663909388, 5.309964801958091840, -3.802871176606228865 ) ) ;
#17879=CARTESIAN_POINT ( 'NONE',  ( 0.2565376335216897341, -2.516992571280221913, -6.500000000000063949 ) ) ;
#17896=DIRECTION ( 'NONE',  ( 0.000000000000000000, -5.551115123125748189E-17, -1.000000000000000000 ) ) ;
#17911=EDGE_CURVE ( 'NONE', #8947, #10723, #7536, .T. ) ;
#17912=AXIS2_PLACEMENT_3D ( 'NONE', #3265, #1690, #14512 ) ;
#17919=DIRECTION ( 'NONE',  ( 0.000000000000000000, 1.000000000000000000, 2.775557561562874095E-16 ) ) ;
#17955=VECTOR ( 'NONE', #10474, 999.9999999999998863 ) ;
#17972=CARTESIAN_POINT ( 'NONE',  ( 0.2573354458087886432, 6.889406814520515177, -1.067197363239279939 ) ) ;
#17980=AXIS2_PLACEMENT_3D ( 'NONE', #14400, #14496, #12752 ) ;
#18094=EDGE_CURVE ( 'NONE', #850, #17620, #7276, .T. ) ;
#18142=B_SPLINE_CURVE_WITH_KNOTS ( 'NONE', 3,
 ( #9283, #12183, #17873, #15159, #18463, #9842, #14057, #6944 ),
 .UNSPECIFIED., .F., .F.,
 ( 4, 2, 2, 4 ),
 ( 0.003797433802554483605, 0.004743183970586266514, 0.005688934138618047254, 0.007580434474681613070 ),
 .UNSPECIFIED. ) ;
#18148=FACE_OUTER_BOUND ( 'NONE', #171, .T. ) ;
#18175=DIRECTION ( 'NONE',  ( 0.000000000000000000, 5.551115123125748189E-17, 1.000000000000000000 ) ) ;
#18177=ORIENTED_EDGE ( 'NONE', *, *, #15441, .F. ) ;
#18290=ORIENTED_EDGE ( 'NONE', *, *, #128, .F. ) ;
#18326=VERTEX_POINT ( 'NONE', #7667 ) ;
#18336=ORIENTED_EDGE ( 'NONE', *, *, #9742, .F. ) ;
#18347=DIRECTION ( 'NONE',  ( 0.000000000000000000, -5.551115123125747573E-17, -1.000000000000000000 ) ) ;
#18348=EDGE_CURVE ( 'NONE', #646, #17620, #3538, .T. ) ;
#18353=AXIS2_PLACEMENT_3D ( 'NONE', #5230, #15332, #6531 ) ;
#18371=PLANE ( 'NONE',  #15276 ) ;
#18417=ADVANCED_FACE ( 'NONE', ( #6732 ), #18516, .F. ) ;
#18446=PLANE ( 'NONE',  #12884 ) ;
#18463=CARTESIAN_POINT ( 'NONE',  ( 0.1061556211655609594, 4.836380039389402086, -4.623144047065641082 ) ) ;
#18496=CARTESIAN_POINT ( 'NONE',  ( 4.699999999999995737, -3.752776749732712691, -6.500000000000033751 ) ) ;
#18502=CARTESIAN_POINT ( 'NONE',  ( 4.699999999999995737, 6.499999999999901412, 2.428612866367529932E-14 ) ) ;
#18513=CARTESIAN_POINT ( 'NONE',  ( 0.000000000000000000, -5.629165124598996428, -3.250000000000020428 ) ) ;
#18516=PLANE ( 'NONE',  #4283 ) ;
#18560=COLOUR_RGB('Black',0.12,0.14,0.17);
#18561=FILL_AREA_STYLE_COLOUR('',#18560);
#18562=FILL_AREA_STYLE('',(#18561));
#18563=SURFACE_STYLE_FILL_AREA(#18562);
#18564=SURFACE_SIDE_STYLE('',(#18563));
#18565=SURFACE_STYLE_USAGE(.BOTH.,#18564);
#18566=PRESENTATION_STYLE_ASSIGNMENT((#18565));
ENDSEC;
END-ISO-10303-21;
